ISO-10303-21;
HEADER;
/* Generated by software containing ST-Developer
 * from STEP Tools, Inc. (www.steptools.com) 
 */

FILE_DESCRIPTION(
/* description */ ('Rack and pinion manual slide'),
/* implementation_level */ '2;1');

FILE_NAME(
/* name */ 'Captive slot nut.step',
/* time_stamp */ '2026-10-28T03:22:49-07:00',
/* author */ (''),
/* organization */ (''),
/* preprocessor_version */ 'ST-DEVELOPER v20.2',
/* originating_system */ 'Autodesk Translation Framework v15.17.0.0',
/* authorisation */ '');

FILE_SCHEMA (('AUTOMOTIVE_DESIGN { 1 0 10303 214 3 1 1 }'));
ENDSEC;

DATA;
#10=MECHANICAL_DESIGN_GEOMETRIC_PRESENTATION_REPRESENTATION('',(#747),#34851);
#638=ELLIPSE('',#14688,0.299389011154384,0.2117);
#639=ELLIPSE('',#14692,0.299389011154384,0.2117);
#655=SHAPE_REPRESENTATION_RELATIONSHIP('SRR','None',#35090,#701);
#701=ADVANCED_BREP_SHAPE_REPRESENTATION('',(#800),#34815);
#747=STYLED_ITEM('',(#35418),#800);
#800=MANIFOLD_SOLID_BREP('Body1',#13767);
#959=FACE_BOUND('',#2604,.T.);
#1174=PLANE('',#14678);
#1175=PLANE('',#14679);
#1176=PLANE('',#14680);
#1177=PLANE('',#14682);
#1178=PLANE('',#14683);
#1179=PLANE('',#14684);
#1180=PLANE('',#14685);
#1181=PLANE('',#14686);
#1182=PLANE('',#14687);
#1183=PLANE('',#14694);
#1184=PLANE('',#14695);
#1185=PLANE('',#14696);
#1186=PLANE('',#14697);
#1736=FACE_OUTER_BOUND('',#2601,.T.);
#1737=FACE_OUTER_BOUND('',#2602,.T.);
#1738=FACE_OUTER_BOUND('',#2603,.T.);
#1739=FACE_OUTER_BOUND('',#2605,.T.);
#1740=FACE_OUTER_BOUND('',#2606,.T.);
#1741=FACE_OUTER_BOUND('',#2607,.T.);
#1742=FACE_OUTER_BOUND('',#2608,.T.);
#1743=FACE_OUTER_BOUND('',#2609,.T.);
#1744=FACE_OUTER_BOUND('',#2610,.T.);
#1745=FACE_OUTER_BOUND('',#2611,.T.);
#1746=FACE_OUTER_BOUND('',#2612,.T.);
#1747=FACE_OUTER_BOUND('',#2613,.T.);
#1748=FACE_OUTER_BOUND('',#2614,.T.);
#1749=FACE_OUTER_BOUND('',#2615,.T.);
#2601=EDGE_LOOP('',(#10212,#10213,#10214,#10215));
#2602=EDGE_LOOP('',(#10216,#10217,#10218,#10219));
#2603=EDGE_LOOP('',(#10220,#10221,#10222,#10223));
#2604=EDGE_LOOP('',(#10224));
#2605=EDGE_LOOP('',(#10225,#10226,#10227,#10228,#10229,#10230,#10231,#10232,
#10233,#10234));
#2606=EDGE_LOOP('',(#10235,#10236,#10237,#10238));
#2607=EDGE_LOOP('',(#10239,#10240,#10241,#10242));
#2608=EDGE_LOOP('',(#10243,#10244,#10245,#10246,#10247,#10248,#10249,#10250,
#10251,#10252));
#2609=EDGE_LOOP('',(#10253,#10254,#10255,#10256));
#2610=EDGE_LOOP('',(#10257,#10258,#10259,#10260,#10261,#10262));
#2611=EDGE_LOOP('',(#10263,#10264,#10265,#10266,#10267,#10268,#10269,#10270));
#2612=EDGE_LOOP('',(#10271,#10272,#10273,#10274,#10275));
#2613=EDGE_LOOP('',(#10276,#10277,#10278,#10279));
#2614=EDGE_LOOP('',(#10280,#10281,#10282,#10283,#10284,#10285));
#2615=EDGE_LOOP('',(#10286,#10287,#10288,#10289));
#3571=LINE('',#20494,#4862);
#3572=LINE('',#20496,#4863);
#3573=LINE('',#20498,#4864);
#3574=LINE('',#20499,#4865);
#3575=LINE('',#20502,#4866);
#3576=LINE('',#20504,#4867);
#3577=LINE('',#20505,#4868);
#3578=LINE('',#20508,#4869);
#3579=LINE('',#20510,#4870);
#3580=LINE('',#20511,#4871);
#3581=LINE('',#20516,#4872);
#3582=LINE('',#20518,#4873);
#3583=LINE('',#20520,#4874);
#3584=LINE('',#20522,#4875);
#3585=LINE('',#20524,#4876);
#3586=LINE('',#20526,#4877);
#3587=LINE('',#20527,#4878);
#3588=LINE('',#20530,#4879);
#3589=LINE('',#20531,#4880);
#3590=LINE('',#20534,#4881);
#3591=LINE('',#20535,#4882);
#3592=LINE('',#20538,#4883);
#3593=LINE('',#20540,#4884);
#3594=LINE('',#20542,#4885);
#3595=LINE('',#20544,#4886);
#3596=LINE('',#20545,#4887);
#3597=LINE('',#20547,#4888);
#3598=LINE('',#20550,#4889);
#3599=LINE('',#20553,#4890);
#3600=LINE('',#20557,#4891);
#3601=LINE('',#20564,#4892);
#3602=LINE('',#20566,#4893);
#3603=LINE('',#20568,#4894);
#4862=VECTOR('',#16671,1.);
#4863=VECTOR('',#16672,1.);
#4864=VECTOR('',#16673,1.);
#4865=VECTOR('',#16674,1.);
#4866=VECTOR('',#16677,1.);
#4867=VECTOR('',#16678,1.);
#4868=VECTOR('',#16679,1.);
#4869=VECTOR('',#16682,1.);
#4870=VECTOR('',#16683,1.);
#4871=VECTOR('',#16684,1.);
#4872=VECTOR('',#16689,1.);
#4873=VECTOR('',#16690,1.);
#4874=VECTOR('',#16691,1.);
#4875=VECTOR('',#16692,1.);
#4876=VECTOR('',#16693,1.);
#4877=VECTOR('',#16694,1.);
#4878=VECTOR('',#16695,1.);
#4879=VECTOR('',#16698,1.);
#4880=VECTOR('',#16699,1.);
#4881=VECTOR('',#16702,1.);
#4882=VECTOR('',#16703,1.);
#4883=VECTOR('',#16706,1.);
#4884=VECTOR('',#16707,1.);
#4885=VECTOR('',#16708,1.);
#4886=VECTOR('',#16709,1.);
#4887=VECTOR('',#16710,1.);
#4888=VECTOR('',#16713,1.);
#4889=VECTOR('',#16716,1.);
#4890=VECTOR('',#16719,1.);
#4891=VECTOR('',#16724,0.21);
#4892=VECTOR('',#16733,1.);
#4893=VECTOR('',#16736,1.);
#4894=VECTOR('',#16739,1.);
#5948=CIRCLE('',#14681,0.2117);
#5949=CIRCLE('',#14690,0.2117);
#5950=CIRCLE('',#14691,0.2117);
#5951=CIRCLE('',#14693,0.2117);
#6550=VERTEX_POINT('',#20492);
#6551=VERTEX_POINT('',#20493);
#6552=VERTEX_POINT('',#20495);
#6553=VERTEX_POINT('',#20497);
#6554=VERTEX_POINT('',#20501);
#6555=VERTEX_POINT('',#20503);
#6556=VERTEX_POINT('',#20507);
#6557=VERTEX_POINT('',#20509);
#6558=VERTEX_POINT('',#20512);
#6559=VERTEX_POINT('',#20515);
#6560=VERTEX_POINT('',#20517);
#6561=VERTEX_POINT('',#20519);
#6562=VERTEX_POINT('',#20521);
#6563=VERTEX_POINT('',#20523);
#6564=VERTEX_POINT('',#20525);
#6565=VERTEX_POINT('',#20529);
#6566=VERTEX_POINT('',#20533);
#6567=VERTEX_POINT('',#20537);
#6568=VERTEX_POINT('',#20539);
#6569=VERTEX_POINT('',#20541);
#6570=VERTEX_POINT('',#20543);
#6571=VERTEX_POINT('',#20549);
#6572=VERTEX_POINT('',#20551);
#6573=VERTEX_POINT('',#20555);
#6574=VERTEX_POINT('',#20558);
#6575=VERTEX_POINT('',#20560);
#7918=EDGE_CURVE('',#6550,#6551,#3571,.T.);
#7919=EDGE_CURVE('',#6552,#6550,#3572,.T.);
#7920=EDGE_CURVE('',#6553,#6552,#3573,.T.);
#7921=EDGE_CURVE('',#6551,#6553,#3574,.T.);
#7922=EDGE_CURVE('',#6552,#6554,#3575,.T.);
#7923=EDGE_CURVE('',#6555,#6554,#3576,.T.);
#7924=EDGE_CURVE('',#6553,#6555,#3577,.T.);
#7925=EDGE_CURVE('',#6554,#6556,#3578,.T.);
#7926=EDGE_CURVE('',#6556,#6557,#3579,.T.);
#7927=EDGE_CURVE('',#6557,#6555,#3580,.T.);
#7928=EDGE_CURVE('',#6558,#6558,#5948,.T.);
#7929=EDGE_CURVE('',#6559,#6550,#3581,.T.);
#7930=EDGE_CURVE('',#6560,#6559,#3582,.T.);
#7931=EDGE_CURVE('',#6560,#6561,#3583,.T.);
#7932=EDGE_CURVE('',#6562,#6561,#3584,.T.);
#7933=EDGE_CURVE('',#6562,#6563,#3585,.T.);
#7934=EDGE_CURVE('',#6563,#6564,#3586,.T.);
#7935=EDGE_CURVE('',#6564,#6556,#3587,.T.);
#7936=EDGE_CURVE('',#6564,#6565,#3588,.T.);
#7937=EDGE_CURVE('',#6565,#6557,#3589,.T.);
#7938=EDGE_CURVE('',#6566,#6563,#3590,.T.);
#7939=EDGE_CURVE('',#6565,#6566,#3591,.T.);
#7940=EDGE_CURVE('',#6567,#6566,#3592,.T.);
#7941=EDGE_CURVE('',#6568,#6567,#3593,.T.);
#7942=EDGE_CURVE('',#6568,#6569,#3594,.T.);
#7943=EDGE_CURVE('',#6570,#6569,#3595,.T.);
#7944=EDGE_CURVE('',#6570,#6551,#3596,.T.);
#7945=EDGE_CURVE('',#6567,#6562,#3597,.T.);
#7946=EDGE_CURVE('',#6561,#6571,#3598,.T.);
#7947=EDGE_CURVE('',#6571,#6572,#638,.T.);
#7948=EDGE_CURVE('',#6572,#6568,#3599,.T.);
#7949=EDGE_CURVE('',#6573,#6571,#5949,.F.);
#7950=EDGE_CURVE('',#6573,#6558,#3600,.T.);
#7951=EDGE_CURVE('',#6574,#6573,#5950,.F.);
#7952=EDGE_CURVE('',#6575,#6574,#639,.T.);
#7953=EDGE_CURVE('',#6572,#6575,#5951,.F.);
#7954=EDGE_CURVE('',#6574,#6560,#3601,.T.);
#7955=EDGE_CURVE('',#6569,#6575,#3602,.T.);
#7956=EDGE_CURVE('',#6559,#6570,#3603,.T.);
#10212=ORIENTED_EDGE('',*,*,#7918,.F.);
#10213=ORIENTED_EDGE('',*,*,#7919,.F.);
#10214=ORIENTED_EDGE('',*,*,#7920,.F.);
#10215=ORIENTED_EDGE('',*,*,#7921,.F.);
#10216=ORIENTED_EDGE('',*,*,#7920,.T.);
#10217=ORIENTED_EDGE('',*,*,#7922,.T.);
#10218=ORIENTED_EDGE('',*,*,#7923,.F.);
#10219=ORIENTED_EDGE('',*,*,#7924,.F.);
#10220=ORIENTED_EDGE('',*,*,#7925,.T.);
#10221=ORIENTED_EDGE('',*,*,#7926,.T.);
#10222=ORIENTED_EDGE('',*,*,#7927,.T.);
#10223=ORIENTED_EDGE('',*,*,#7923,.T.);
#10224=ORIENTED_EDGE('',*,*,#7928,.T.);
#10225=ORIENTED_EDGE('',*,*,#7925,.F.);
#10226=ORIENTED_EDGE('',*,*,#7922,.F.);
#10227=ORIENTED_EDGE('',*,*,#7919,.T.);
#10228=ORIENTED_EDGE('',*,*,#7929,.F.);
#10229=ORIENTED_EDGE('',*,*,#7930,.F.);
#10230=ORIENTED_EDGE('',*,*,#7931,.T.);
#10231=ORIENTED_EDGE('',*,*,#7932,.F.);
#10232=ORIENTED_EDGE('',*,*,#7933,.T.);
#10233=ORIENTED_EDGE('',*,*,#7934,.T.);
#10234=ORIENTED_EDGE('',*,*,#7935,.T.);
#10235=ORIENTED_EDGE('',*,*,#7936,.T.);
#10236=ORIENTED_EDGE('',*,*,#7937,.T.);
#10237=ORIENTED_EDGE('',*,*,#7926,.F.);
#10238=ORIENTED_EDGE('',*,*,#7935,.F.);
#10239=ORIENTED_EDGE('',*,*,#7938,.F.);
#10240=ORIENTED_EDGE('',*,*,#7939,.F.);
#10241=ORIENTED_EDGE('',*,*,#7936,.F.);
#10242=ORIENTED_EDGE('',*,*,#7934,.F.);
#10243=ORIENTED_EDGE('',*,*,#7927,.F.);
#10244=ORIENTED_EDGE('',*,*,#7937,.F.);
#10245=ORIENTED_EDGE('',*,*,#7939,.T.);
#10246=ORIENTED_EDGE('',*,*,#7940,.F.);
#10247=ORIENTED_EDGE('',*,*,#7941,.F.);
#10248=ORIENTED_EDGE('',*,*,#7942,.T.);
#10249=ORIENTED_EDGE('',*,*,#7943,.F.);
#10250=ORIENTED_EDGE('',*,*,#7944,.T.);
#10251=ORIENTED_EDGE('',*,*,#7921,.T.);
#10252=ORIENTED_EDGE('',*,*,#7924,.T.);
#10253=ORIENTED_EDGE('',*,*,#7938,.T.);
#10254=ORIENTED_EDGE('',*,*,#7933,.F.);
#10255=ORIENTED_EDGE('',*,*,#7945,.F.);
#10256=ORIENTED_EDGE('',*,*,#7940,.T.);
#10257=ORIENTED_EDGE('',*,*,#7941,.T.);
#10258=ORIENTED_EDGE('',*,*,#7945,.T.);
#10259=ORIENTED_EDGE('',*,*,#7932,.T.);
#10260=ORIENTED_EDGE('',*,*,#7946,.T.);
#10261=ORIENTED_EDGE('',*,*,#7947,.T.);
#10262=ORIENTED_EDGE('',*,*,#7948,.T.);
#10263=ORIENTED_EDGE('',*,*,#7947,.F.);
#10264=ORIENTED_EDGE('',*,*,#7949,.F.);
#10265=ORIENTED_EDGE('',*,*,#7950,.T.);
#10266=ORIENTED_EDGE('',*,*,#7928,.F.);
#10267=ORIENTED_EDGE('',*,*,#7950,.F.);
#10268=ORIENTED_EDGE('',*,*,#7951,.F.);
#10269=ORIENTED_EDGE('',*,*,#7952,.F.);
#10270=ORIENTED_EDGE('',*,*,#7953,.F.);
#10271=ORIENTED_EDGE('',*,*,#7946,.F.);
#10272=ORIENTED_EDGE('',*,*,#7931,.F.);
#10273=ORIENTED_EDGE('',*,*,#7954,.F.);
#10274=ORIENTED_EDGE('',*,*,#7951,.T.);
#10275=ORIENTED_EDGE('',*,*,#7949,.T.);
#10276=ORIENTED_EDGE('',*,*,#7948,.F.);
#10277=ORIENTED_EDGE('',*,*,#7953,.T.);
#10278=ORIENTED_EDGE('',*,*,#7955,.F.);
#10279=ORIENTED_EDGE('',*,*,#7942,.F.);
#10280=ORIENTED_EDGE('',*,*,#7930,.T.);
#10281=ORIENTED_EDGE('',*,*,#7956,.T.);
#10282=ORIENTED_EDGE('',*,*,#7943,.T.);
#10283=ORIENTED_EDGE('',*,*,#7955,.T.);
#10284=ORIENTED_EDGE('',*,*,#7952,.T.);
#10285=ORIENTED_EDGE('',*,*,#7954,.T.);
#10286=ORIENTED_EDGE('',*,*,#7918,.T.);
#10287=ORIENTED_EDGE('',*,*,#7944,.F.);
#10288=ORIENTED_EDGE('',*,*,#7956,.F.);
#10289=ORIENTED_EDGE('',*,*,#7929,.T.);
#12915=CYLINDRICAL_SURFACE('',#14689,0.2117);
#13214=ADVANCED_FACE('',(#1736),#1174,.F.);
#13215=ADVANCED_FACE('',(#1737),#1175,.T.);
#13216=ADVANCED_FACE('',(#1738,#959),#1176,.T.);
#13217=ADVANCED_FACE('',(#1739),#1177,.T.);
#13218=ADVANCED_FACE('',(#1740),#1178,.T.);
#13219=ADVANCED_FACE('',(#1741),#1179,.F.);
#13220=ADVANCED_FACE('',(#1742),#1180,.T.);
#13221=ADVANCED_FACE('',(#1743),#1181,.T.);
#13222=ADVANCED_FACE('',(#1744),#1182,.T.);
#13223=ADVANCED_FACE('',(#1745),#12915,.F.);
#13224=ADVANCED_FACE('',(#1746),#1183,.F.);
#13225=ADVANCED_FACE('',(#1747),#1184,.F.);
#13226=ADVANCED_FACE('',(#1748),#1185,.T.);
#13227=ADVANCED_FACE('',(#1749),#1186,.T.);
#13767=CLOSED_SHELL('',(#13214,#13215,#13216,#13217,#13218,#13219,#13220,
#13221,#13222,#13223,#13224,#13225,#13226,#13227));
#14677=AXIS2_PLACEMENT_3D('',#20490,#16667,#16668);
#14678=AXIS2_PLACEMENT_3D('',#20491,#16669,#16670);
#14679=AXIS2_PLACEMENT_3D('',#20500,#16675,#16676);
#14680=AXIS2_PLACEMENT_3D('',#20506,#16680,#16681);
#14681=AXIS2_PLACEMENT_3D('',#20513,#16685,#16686);
#14682=AXIS2_PLACEMENT_3D('',#20514,#16687,#16688);
#14683=AXIS2_PLACEMENT_3D('',#20528,#16696,#16697);
#14684=AXIS2_PLACEMENT_3D('',#20532,#16700,#16701);
#14685=AXIS2_PLACEMENT_3D('',#20536,#16704,#16705);
#14686=AXIS2_PLACEMENT_3D('',#20546,#16711,#16712);
#14687=AXIS2_PLACEMENT_3D('',#20548,#16714,#16715);
#14688=AXIS2_PLACEMENT_3D('',#20552,#16717,#16718);
#14689=AXIS2_PLACEMENT_3D('',#20554,#16720,#16721);
#14690=AXIS2_PLACEMENT_3D('',#20556,#16722,#16723);
#14691=AXIS2_PLACEMENT_3D('',#20559,#16725,#16726);
#14692=AXIS2_PLACEMENT_3D('',#20561,#16727,#16728);
#14693=AXIS2_PLACEMENT_3D('',#20562,#16729,#16730);
#14694=AXIS2_PLACEMENT_3D('',#20563,#16731,#16732);
#14695=AXIS2_PLACEMENT_3D('',#20565,#16734,#16735);
#14696=AXIS2_PLACEMENT_3D('',#20567,#16737,#16738);
#14697=AXIS2_PLACEMENT_3D('',#20569,#16740,#16741);
#16667=DIRECTION('axis',(0.,0.,1.));
#16668=DIRECTION('refdir',(1.,0.,0.));
#16669=DIRECTION('center_axis',(0.,0.,1.));
#16670=DIRECTION('ref_axis',(1.,0.,0.));
#16671=DIRECTION('',(1.,0.,0.));
#16672=DIRECTION('',(0.,-1.,0.));
#16673=DIRECTION('',(-1.,0.,0.));
#16674=DIRECTION('',(0.,1.,0.));
#16675=DIRECTION('center_axis',(0.,1.,0.));
#16676=DIRECTION('ref_axis',(-1.,0.,0.));
#16677=DIRECTION('',(0.,0.,1.));
#16678=DIRECTION('',(-1.,0.,0.));
#16679=DIRECTION('',(0.,0.,1.));
#16680=DIRECTION('center_axis',(0.,0.,1.));
#16681=DIRECTION('ref_axis',(1.,0.,0.));
#16682=DIRECTION('',(0.,-1.,0.));
#16683=DIRECTION('',(1.,0.,0.));
#16684=DIRECTION('',(0.,1.,0.));
#16685=DIRECTION('center_axis',(0.,0.,-1.));
#16686=DIRECTION('ref_axis',(1.,0.,0.));
#16687=DIRECTION('center_axis',(-1.,0.,0.));
#16688=DIRECTION('ref_axis',(0.,-1.,0.));
#16689=DIRECTION('',(0.,0.,1.));
#16690=DIRECTION('',(0.,0.707106781186548,0.707106781186548));
#16691=DIRECTION('',(0.,-1.,0.));
#16692=DIRECTION('',(0.,0.707106781186548,-0.707106781186548));
#16693=DIRECTION('',(0.,0.,1.));
#16694=DIRECTION('',(0.,-1.,0.));
#16695=DIRECTION('',(0.,0.,1.));
#16696=DIRECTION('center_axis',(0.,-1.,0.));
#16697=DIRECTION('ref_axis',(1.,0.,0.));
#16698=DIRECTION('',(1.,0.,0.));
#16699=DIRECTION('',(0.,0.,1.));
#16700=DIRECTION('center_axis',(0.,0.,1.));
#16701=DIRECTION('ref_axis',(1.,0.,0.));
#16702=DIRECTION('',(-1.,0.,0.));
#16703=DIRECTION('',(0.,1.,0.));
#16704=DIRECTION('center_axis',(1.,0.,0.));
#16705=DIRECTION('ref_axis',(0.,1.,0.));
#16706=DIRECTION('',(0.,0.,1.));
#16707=DIRECTION('',(0.,-0.707106781186548,0.707106781186548));
#16708=DIRECTION('',(0.,1.,0.));
#16709=DIRECTION('',(0.,-0.707106781186548,-0.707106781186548));
#16710=DIRECTION('',(0.,0.,1.));
#16711=DIRECTION('center_axis',(0.,-1.,0.));
#16712=DIRECTION('ref_axis',(1.,0.,0.));
#16713=DIRECTION('',(-1.,0.,0.));
#16714=DIRECTION('center_axis',(0.,-0.707106781186548,-0.707106781186548));
#16715=DIRECTION('ref_axis',(-1.,0.,0.));
#16716=DIRECTION('',(1.,0.,0.));
#16717=DIRECTION('center_axis',(0.,0.707106781186548,0.707106781186548));
#16718=DIRECTION('ref_axis',(0.,0.707106781186547,-0.707106781186547));
#16719=DIRECTION('',(1.,0.,0.));
#16720=DIRECTION('center_axis',(0.,0.,1.));
#16721=DIRECTION('ref_axis',(1.,0.,0.));
#16722=DIRECTION('center_axis',(0.,0.,-1.));
#16723=DIRECTION('ref_axis',(1.,0.,0.));
#16724=DIRECTION('',(0.,0.,1.));
#16725=DIRECTION('center_axis',(0.,0.,-1.));
#16726=DIRECTION('ref_axis',(1.,0.,0.));
#16727=DIRECTION('center_axis',(0.,-0.707106781186548,0.707106781186548));
#16728=DIRECTION('ref_axis',(0.,0.707106781186547,0.707106781186547));
#16729=DIRECTION('center_axis',(0.,0.,-1.));
#16730=DIRECTION('ref_axis',(1.,0.,0.));
#16731=DIRECTION('center_axis',(0.,0.,1.));
#16732=DIRECTION('ref_axis',(1.,0.,0.));
#16733=DIRECTION('',(-1.,0.,0.));
#16734=DIRECTION('center_axis',(0.,0.,1.));
#16735=DIRECTION('ref_axis',(1.,0.,0.));
#16736=DIRECTION('',(-1.,0.,0.));
#16737=DIRECTION('center_axis',(0.,0.707106781186548,-0.707106781186548));
#16738=DIRECTION('ref_axis',(-1.,0.,0.));
#16739=DIRECTION('',(1.,0.,0.));
#16740=DIRECTION('center_axis',(0.,1.,0.));
#16741=DIRECTION('ref_axis',(-1.,0.,0.));
#20490=CARTESIAN_POINT('',(0.,0.,0.));
#20491=CARTESIAN_POINT('Origin',(0.,0.395,0.25));
#20492=CARTESIAN_POINT('',(-0.5,0.3,0.25));
#20493=CARTESIAN_POINT('',(0.5,0.3,0.25));
#20494=CARTESIAN_POINT('',(0.25,0.3,0.25));
#20495=CARTESIAN_POINT('',(-0.5,0.5,0.25));
#20496=CARTESIAN_POINT('',(-0.5,0.5,0.25));
#20497=CARTESIAN_POINT('',(0.5,0.5,0.25));
#20498=CARTESIAN_POINT('',(0.5,0.5,0.25));
#20499=CARTESIAN_POINT('',(0.5,0.29,0.25));
#20500=CARTESIAN_POINT('Origin',(0.5,0.5,0.25));
#20501=CARTESIAN_POINT('',(-0.5,0.5,0.4));
#20502=CARTESIAN_POINT('',(-0.5,0.5,0.25));
#20503=CARTESIAN_POINT('',(0.5,0.5,0.4));
#20504=CARTESIAN_POINT('',(0.5,0.5,0.4));
#20505=CARTESIAN_POINT('',(0.5,0.5,0.25));
#20506=CARTESIAN_POINT('Origin',(0.,0.,0.4));
#20507=CARTESIAN_POINT('',(-0.5,-0.5,0.4));
#20508=CARTESIAN_POINT('',(-0.5,0.5,0.4));
#20509=CARTESIAN_POINT('',(0.5,-0.5,0.4));
#20510=CARTESIAN_POINT('',(-0.5,-0.5,0.4));
#20511=CARTESIAN_POINT('',(0.5,-0.3,0.4));
#20512=CARTESIAN_POINT('',(-0.2117,2.59257727379495E-17,0.4));
#20513=CARTESIAN_POINT('Origin',(0.,0.,0.4));
#20514=CARTESIAN_POINT('Origin',(-0.5,0.3,0.));
#20515=CARTESIAN_POINT('',(-0.5,0.3,0.15));
#20516=CARTESIAN_POINT('',(-0.5,0.3,0.));
#20517=CARTESIAN_POINT('',(-0.5,0.15,0.));
#20518=CARTESIAN_POINT('',(-0.5,0.225,0.075));
#20519=CARTESIAN_POINT('',(-0.5,-0.15,0.));
#20520=CARTESIAN_POINT('',(-0.5,0.3,0.));
#20521=CARTESIAN_POINT('',(-0.5,-0.3,0.15));
#20522=CARTESIAN_POINT('',(-0.5,-0.075,-0.075));
#20523=CARTESIAN_POINT('',(-0.5,-0.3,0.25));
#20524=CARTESIAN_POINT('',(-0.5,-0.3,0.));
#20525=CARTESIAN_POINT('',(-0.5,-0.5,0.25));
#20526=CARTESIAN_POINT('',(-0.5,-0.29,0.25));
#20527=CARTESIAN_POINT('',(-0.5,-0.5,0.25));
#20528=CARTESIAN_POINT('Origin',(-0.5,-0.5,0.25));
#20529=CARTESIAN_POINT('',(0.5,-0.5,0.25));
#20530=CARTESIAN_POINT('',(-0.5,-0.5,0.25));
#20531=CARTESIAN_POINT('',(0.5,-0.5,0.25));
#20532=CARTESIAN_POINT('Origin',(0.,-0.395,0.25));
#20533=CARTESIAN_POINT('',(0.5,-0.3,0.25));
#20534=CARTESIAN_POINT('',(-0.25,-0.3,0.25));
#20535=CARTESIAN_POINT('',(0.5,-0.5,0.25));
#20536=CARTESIAN_POINT('Origin',(0.5,-0.3,0.));
#20537=CARTESIAN_POINT('',(0.5,-0.3,0.15));
#20538=CARTESIAN_POINT('',(0.5,-0.3,0.));
#20539=CARTESIAN_POINT('',(0.5,-0.15,0.));
#20540=CARTESIAN_POINT('',(0.5,-0.225,0.075));
#20541=CARTESIAN_POINT('',(0.5,0.15,0.));
#20542=CARTESIAN_POINT('',(0.5,-0.3,0.));
#20543=CARTESIAN_POINT('',(0.5,0.3,0.15));
#20544=CARTESIAN_POINT('',(0.5,0.075,-0.075));
#20545=CARTESIAN_POINT('',(0.5,0.3,0.));
#20546=CARTESIAN_POINT('Origin',(-0.5,-0.3,0.));
#20547=CARTESIAN_POINT('',(-0.25,-0.3,0.15));
#20548=CARTESIAN_POINT('Origin',(-0.25,-0.225,0.075));
#20549=CARTESIAN_POINT('',(-0.149388386429468,-0.15,0.));
#20550=CARTESIAN_POINT('',(-0.25,-0.15,0.));
#20551=CARTESIAN_POINT('',(0.149388386429468,-0.15,0.));
#20552=CARTESIAN_POINT('Origin',(0.,0.,-0.15));
#20553=CARTESIAN_POINT('',(-0.25,-0.15,0.));
#20554=CARTESIAN_POINT('Origin',(0.,0.,-0.1));
#20555=CARTESIAN_POINT('',(-0.2117,-2.59257727379495E-17,0.));
#20556=CARTESIAN_POINT('Origin',(0.,0.,0.));
#20557=CARTESIAN_POINT('',(-0.2117,-2.59257727379495E-17,-0.1));
#20558=CARTESIAN_POINT('',(-0.149388386429468,0.15,0.));
#20559=CARTESIAN_POINT('Origin',(0.,0.,0.));
#20560=CARTESIAN_POINT('',(0.149388386429468,0.15,0.));
#20561=CARTESIAN_POINT('Origin',(0.,0.,-0.15));
#20562=CARTESIAN_POINT('Origin',(0.,0.,0.));
#20563=CARTESIAN_POINT('Origin',(0.,0.,0.));
#20564=CARTESIAN_POINT('',(0.25,0.15,0.));
#20565=CARTESIAN_POINT('Origin',(0.,0.,0.));
#20566=CARTESIAN_POINT('',(0.25,0.15,0.));
#20567=CARTESIAN_POINT('Origin',(0.25,0.225,0.075));
#20568=CARTESIAN_POINT('',(0.25,0.3,0.15));
#20569=CARTESIAN_POINT('Origin',(0.5,0.3,0.));
#34761=UNCERTAINTY_MEASURE_WITH_UNIT(LENGTH_MEASURE(0.001),#34852,
'DISTANCE_ACCURACY_VALUE',
'Maximum model space distance between geometric entities at asserted c
onnectivities');
#34797=UNCERTAINTY_MEASURE_WITH_UNIT(LENGTH_MEASURE(0.001),#34852,
'DISTANCE_ACCURACY_VALUE',
'Maximum model space distance between geometric entities at asserted c
onnectivities');
#34815=(
GEOMETRIC_REPRESENTATION_CONTEXT(3)
GLOBAL_UNCERTAINTY_ASSIGNED_CONTEXT((#34761))
GLOBAL_UNIT_ASSIGNED_CONTEXT((#34852,#34854,#34855))
REPRESENTATION_CONTEXT('','3D')
);
#34851=(
GEOMETRIC_REPRESENTATION_CONTEXT(3)
GLOBAL_UNCERTAINTY_ASSIGNED_CONTEXT((#34797))
GLOBAL_UNIT_ASSIGNED_CONTEXT((#34852,#34854,#34855))
REPRESENTATION_CONTEXT('','3D')
);
#34852=(
LENGTH_UNIT()
NAMED_UNIT(*)
SI_UNIT(.CENTI.,.METRE.)
);
#34854=(
NAMED_UNIT(*)
PLANE_ANGLE_UNIT()
SI_UNIT($,.RADIAN.)
);
#34855=(
NAMED_UNIT(*)
SI_UNIT($,.STERADIAN.)
SOLID_ANGLE_UNIT()
);
#34873=SHAPE_DEFINITION_REPRESENTATION(#34926,#35090);
#34926=PRODUCT_DEFINITION_SHAPE('',$,#35144);
#35090=SHAPE_REPRESENTATION('',(#14677),#34815);
#35126=PRODUCT_DEFINITION_CONTEXT('part definition',#35287,'design');
#35144=PRODUCT_DEFINITION('Captive slot nut','Captive slot nut',#35197,
#35126);
#35197=PRODUCT_DEFINITION_FORMATION('',$,#35306);
#35287=APPLICATION_CONTEXT(
'Core Data for Automotive Mechanical Design Process');
#35288=PRODUCT_CONTEXT('part definition',#35287,'mechanical');
#35306=PRODUCT('Captive slot nut','Captive slot nut','Captive slot nut',
(#35288));
#35412=COLOUR_RGB('Black',0.12,0.14,0.17);
#35413=FILL_AREA_STYLE_COLOUR('',#35412);
#35414=FILL_AREA_STYLE('',(#35413));
#35415=SURFACE_STYLE_FILL_AREA(#35414);
#35416=SURFACE_SIDE_STYLE('',(#35415));
#35417=SURFACE_STYLE_USAGE(.BOTH.,#35416);
#35418=PRESENTATION_STYLE_ASSIGNMENT((#35417));
ENDSEC;
END-ISO-10303-21;
